ISO-10303-21;
HEADER;
/* Generated by software containing ST-Developer
 * from STEP Tools, Inc. (www.steptools.com) 
 */

FILE_DESCRIPTION(
/* description */ (''),
/* implementation_level */ '2;1');

FILE_NAME(
/* name */ 'Blade_03.step',
/* time_stamp */ '2026-10-23T22:28:14+06:00',
/* author */ (''),
/* organization */ (''),
/* preprocessor_version */ 'ST-DEVELOPER v20.2',
/* originating_system */ 'Autodesk Translation Framework v15.15.0.0',
/* authorisation */ '');

FILE_SCHEMA (('AUTOMOTIVE_DESIGN { 1 0 10303 214 3 1 1 }'));
ENDSEC;

DATA;
#10=MECHANICAL_DESIGN_GEOMETRIC_PRESENTATION_REPRESENTATION('',(#110),#6753);
#84=SHAPE_REPRESENTATION_RELATIONSHIP('SRR','None',#6807,#97);
#97=ADVANCED_BREP_SHAPE_REPRESENTATION('',(#123),#6747);
#110=STYLED_ITEM('',(#6914),#123);
#123=MANIFOLD_SOLID_BREP('Blade_03',#3759);
#174=FACE_BOUND('',#747,.T.);
#175=FACE_BOUND('',#748,.T.);
#297=PLANE('',#4239);
#298=PLANE('',#4240);
#299=PLANE('',#4241);
#300=PLANE('',#4248);
#301=PLANE('',#4251);
#302=PLANE('',#4256);
#486=FACE_OUTER_BOUND('',#744,.T.);
#487=FACE_OUTER_BOUND('',#745,.T.);
#488=FACE_OUTER_BOUND('',#746,.T.);
#489=FACE_OUTER_BOUND('',#749,.T.);
#490=FACE_OUTER_BOUND('',#750,.T.);
#491=FACE_OUTER_BOUND('',#751,.T.);
#492=FACE_OUTER_BOUND('',#752,.T.);
#493=FACE_OUTER_BOUND('',#753,.T.);
#494=FACE_OUTER_BOUND('',#754,.T.);
#495=FACE_OUTER_BOUND('',#755,.T.);
#744=EDGE_LOOP('',(#3262,#3263,#3264,#3265));
#745=EDGE_LOOP('',(#3266,#3267,#3268,#3269));
#746=EDGE_LOOP('',(#3270,#3271,#3272,#3273));
#747=EDGE_LOOP('',(#3274));
#748=EDGE_LOOP('',(#3275));
#749=EDGE_LOOP('',(#3276,#3277,#3278,#3279));
#750=EDGE_LOOP('',(#3280));
#751=EDGE_LOOP('',(#3281,#3282,#3283,#3284));
#752=EDGE_LOOP('',(#3285));
#753=EDGE_LOOP('',(#3286,#3287,#3288,#3289));
#754=EDGE_LOOP('',(#3290,#3291,#3292,#3293));
#755=EDGE_LOOP('',(#3294,#3295,#3296,#3297));
#984=CIRCLE('',#4242,33.8);
#985=CIRCLE('',#4243,4.99999999999999);
#986=CIRCLE('',#4244,1.1);
#987=CIRCLE('',#4245,1.1);
#988=CIRCLE('',#4247,1.1);
#989=CIRCLE('',#4250,1.1);
#990=CIRCLE('',#4253,4.99999999999999);
#991=CIRCLE('',#4255,33.8);
#1258=LINE('',#6469,#1544);
#1259=LINE('',#6471,#1545);
#1260=LINE('',#6473,#1546);
#1261=LINE('',#6474,#1547);
#1262=LINE('',#6478,#1548);
#1263=LINE('',#6480,#1549);
#1264=LINE('',#6482,#1550);
#1265=LINE('',#6483,#1551);
#1266=LINE('',#6494,#1552);
#1267=LINE('',#6499,#1553);
#1544=VECTOR('',#5253,10.);
#1545=VECTOR('',#5254,10.);
#1546=VECTOR('',#5255,10.);
#1547=VECTOR('',#5256,10.);
#1548=VECTOR('',#5259,10.);
#1549=VECTOR('',#5260,10.);
#1550=VECTOR('',#5261,10.);
#1551=VECTOR('',#5262,10.);
#1552=VECTOR('',#5277,1.1);
#1553=VECTOR('',#5284,1.1);
#1873=VERTEX_POINT('',#6467);
#1874=VERTEX_POINT('',#6468);
#1875=VERTEX_POINT('',#6470);
#1876=VERTEX_POINT('',#6472);
#1877=VERTEX_POINT('',#6476);
#1878=VERTEX_POINT('',#6477);
#1879=VERTEX_POINT('',#6479);
#1880=VERTEX_POINT('',#6481);
#1881=VERTEX_POINT('',#6487);
#1882=VERTEX_POINT('',#6489);
#1883=VERTEX_POINT('',#6492);
#1884=VERTEX_POINT('',#6497);
#2348=EDGE_CURVE('',#1873,#1874,#1258,.T.);
#2349=EDGE_CURVE('',#1875,#1873,#1259,.T.);
#2350=EDGE_CURVE('',#1876,#1875,#1260,.T.);
#2351=EDGE_CURVE('',#1874,#1876,#1261,.T.);
#2352=EDGE_CURVE('',#1877,#1878,#1262,.T.);
#2353=EDGE_CURVE('',#1879,#1877,#1263,.T.);
#2354=EDGE_CURVE('',#1880,#1879,#1264,.T.);
#2355=EDGE_CURVE('',#1878,#1880,#1265,.T.);
#2356=EDGE_CURVE('',#1877,#1874,#984,.T.);
#2357=EDGE_CURVE('',#1873,#1878,#985,.T.);
#2358=EDGE_CURVE('',#1881,#1881,#986,.T.);
#2359=EDGE_CURVE('',#1882,#1882,#987,.T.);
#2360=EDGE_CURVE('',#1883,#1883,#988,.T.);
#2361=EDGE_CURVE('',#1883,#1881,#1266,.T.);
#2362=EDGE_CURVE('',#1884,#1884,#989,.T.);
#2363=EDGE_CURVE('',#1884,#1882,#1267,.T.);
#2364=EDGE_CURVE('',#1875,#1880,#990,.T.);
#2365=EDGE_CURVE('',#1879,#1876,#991,.T.);
#3262=ORIENTED_EDGE('',*,*,#2348,.F.);
#3263=ORIENTED_EDGE('',*,*,#2349,.F.);
#3264=ORIENTED_EDGE('',*,*,#2350,.F.);
#3265=ORIENTED_EDGE('',*,*,#2351,.F.);
#3266=ORIENTED_EDGE('',*,*,#2352,.F.);
#3267=ORIENTED_EDGE('',*,*,#2353,.F.);
#3268=ORIENTED_EDGE('',*,*,#2354,.F.);
#3269=ORIENTED_EDGE('',*,*,#2355,.F.);
#3270=ORIENTED_EDGE('',*,*,#2348,.T.);
#3271=ORIENTED_EDGE('',*,*,#2356,.F.);
#3272=ORIENTED_EDGE('',*,*,#2352,.T.);
#3273=ORIENTED_EDGE('',*,*,#2357,.F.);
#3274=ORIENTED_EDGE('',*,*,#2358,.T.);
#3275=ORIENTED_EDGE('',*,*,#2359,.T.);
#3276=ORIENTED_EDGE('',*,*,#2360,.F.);
#3277=ORIENTED_EDGE('',*,*,#2361,.T.);
#3278=ORIENTED_EDGE('',*,*,#2358,.F.);
#3279=ORIENTED_EDGE('',*,*,#2361,.F.);
#3280=ORIENTED_EDGE('',*,*,#2360,.T.);
#3281=ORIENTED_EDGE('',*,*,#2362,.F.);
#3282=ORIENTED_EDGE('',*,*,#2363,.T.);
#3283=ORIENTED_EDGE('',*,*,#2359,.F.);
#3284=ORIENTED_EDGE('',*,*,#2363,.F.);
#3285=ORIENTED_EDGE('',*,*,#2362,.T.);
#3286=ORIENTED_EDGE('',*,*,#2349,.T.);
#3287=ORIENTED_EDGE('',*,*,#2357,.T.);
#3288=ORIENTED_EDGE('',*,*,#2355,.T.);
#3289=ORIENTED_EDGE('',*,*,#2364,.F.);
#3290=ORIENTED_EDGE('',*,*,#2351,.T.);
#3291=ORIENTED_EDGE('',*,*,#2365,.F.);
#3292=ORIENTED_EDGE('',*,*,#2353,.T.);
#3293=ORIENTED_EDGE('',*,*,#2356,.T.);
#3294=ORIENTED_EDGE('',*,*,#2350,.T.);
#3295=ORIENTED_EDGE('',*,*,#2364,.T.);
#3296=ORIENTED_EDGE('',*,*,#2354,.T.);
#3297=ORIENTED_EDGE('',*,*,#2365,.T.);
#3515=CYLINDRICAL_SURFACE('',#4246,1.1);
#3516=CYLINDRICAL_SURFACE('',#4249,1.1);
#3517=CYLINDRICAL_SURFACE('',#4252,4.99999999999999);
#3518=CYLINDRICAL_SURFACE('',#4254,33.8);
#3692=ADVANCED_FACE('',(#486),#297,.F.);
#3693=ADVANCED_FACE('',(#487),#298,.F.);
#3694=ADVANCED_FACE('',(#488,#174,#175),#299,.F.);
#3695=ADVANCED_FACE('',(#489),#3515,.T.);
#3696=ADVANCED_FACE('',(#490),#300,.F.);
#3697=ADVANCED_FACE('',(#491),#3516,.T.);
#3698=ADVANCED_FACE('',(#492),#301,.F.);
#3699=ADVANCED_FACE('',(#493),#3517,.F.);
#3700=ADVANCED_FACE('',(#494),#3518,.T.);
#3701=ADVANCED_FACE('',(#495),#302,.T.);
#3759=CLOSED_SHELL('',(#3692,#3693,#3694,#3695,#3696,#3697,#3698,#3699,
#3700,#3701));
#4238=AXIS2_PLACEMENT_3D('',#6465,#5249,#5250);
#4239=AXIS2_PLACEMENT_3D('',#6466,#5251,#5252);
#4240=AXIS2_PLACEMENT_3D('',#6475,#5257,#5258);
#4241=AXIS2_PLACEMENT_3D('',#6484,#5263,#5264);
#4242=AXIS2_PLACEMENT_3D('',#6485,#5265,#5266);
#4243=AXIS2_PLACEMENT_3D('',#6486,#5267,#5268);
#4244=AXIS2_PLACEMENT_3D('',#6488,#5269,#5270);
#4245=AXIS2_PLACEMENT_3D('',#6490,#5271,#5272);
#4246=AXIS2_PLACEMENT_3D('',#6491,#5273,#5274);
#4247=AXIS2_PLACEMENT_3D('',#6493,#5275,#5276);
#4248=AXIS2_PLACEMENT_3D('',#6495,#5278,#5279);
#4249=AXIS2_PLACEMENT_3D('',#6496,#5280,#5281);
#4250=AXIS2_PLACEMENT_3D('',#6498,#5282,#5283);
#4251=AXIS2_PLACEMENT_3D('',#6500,#5285,#5286);
#4252=AXIS2_PLACEMENT_3D('',#6501,#5287,#5288);
#4253=AXIS2_PLACEMENT_3D('',#6502,#5289,#5290);
#4254=AXIS2_PLACEMENT_3D('',#6503,#5291,#5292);
#4255=AXIS2_PLACEMENT_3D('',#6504,#5293,#5294);
#4256=AXIS2_PLACEMENT_3D('',#6505,#5295,#5296);
#5249=DIRECTION('axis',(0.,0.,1.));
#5250=DIRECTION('refdir',(1.,0.,0.));
#5251=DIRECTION('center_axis',(-0.707106781186548,0.,-0.707106781186547));
#5252=DIRECTION('ref_axis',(-0.707106781186547,0.,0.707106781186548));
#5253=DIRECTION('',(-0.707106781186547,0.,0.707106781186548));
#5254=DIRECTION('',(0.,-1.,0.));
#5255=DIRECTION('',(0.707106781186547,0.,-0.707106781186548));
#5256=DIRECTION('',(0.,1.,0.));
#5257=DIRECTION('center_axis',(6.12323399573677E-17,0.,1.));
#5258=DIRECTION('ref_axis',(1.,0.,-6.12323399573677E-17));
#5259=DIRECTION('',(1.,0.,-6.12323399573677E-17));
#5260=DIRECTION('',(0.,-1.,0.));
#5261=DIRECTION('',(-1.,0.,6.12323399573677E-17));
#5262=DIRECTION('',(0.,1.,0.));
#5263=DIRECTION('center_axis',(0.,1.,0.));
#5264=DIRECTION('ref_axis',(6.12323399573677E-17,0.,1.));
#5265=DIRECTION('center_axis',(0.,1.,0.));
#5266=DIRECTION('ref_axis',(6.12323399573677E-17,0.,1.));
#5267=DIRECTION('center_axis',(0.,-1.,0.));
#5268=DIRECTION('ref_axis',(6.12323399573676E-17,0.,1.));
#5269=DIRECTION('center_axis',(0.,1.,0.));
#5270=DIRECTION('ref_axis',(6.12323399573677E-17,0.,1.));
#5271=DIRECTION('center_axis',(0.,1.,0.));
#5272=DIRECTION('ref_axis',(6.12323399573677E-17,0.,1.));
#5273=DIRECTION('center_axis',(0.,-1.,0.));
#5274=DIRECTION('ref_axis',(6.12323399573677E-17,0.,1.));
#5275=DIRECTION('center_axis',(0.,-1.,0.));
#5276=DIRECTION('ref_axis',(6.12323399573677E-17,0.,1.));
#5277=DIRECTION('',(0.,1.,0.));
#5278=DIRECTION('center_axis',(0.,1.,0.));
#5279=DIRECTION('ref_axis',(6.12323399573677E-17,0.,1.));
#5280=DIRECTION('center_axis',(0.,-1.,0.));
#5281=DIRECTION('ref_axis',(6.12323399573677E-17,0.,1.));
#5282=DIRECTION('center_axis',(0.,-1.,0.));
#5283=DIRECTION('ref_axis',(6.12323399573677E-17,0.,1.));
#5284=DIRECTION('',(0.,1.,0.));
#5285=DIRECTION('center_axis',(0.,1.,0.));
#5286=DIRECTION('ref_axis',(6.12323399573677E-17,0.,1.));
#5287=DIRECTION('center_axis',(0.,1.,0.));
#5288=DIRECTION('ref_axis',(6.12323399573676E-17,0.,1.));
#5289=DIRECTION('center_axis',(0.,-1.,0.));
#5290=DIRECTION('ref_axis',(6.12323399573676E-17,0.,1.));
#5291=DIRECTION('center_axis',(0.,1.,0.));
#5292=DIRECTION('ref_axis',(6.12323399573677E-17,0.,1.));
#5293=DIRECTION('center_axis',(0.,1.,0.));
#5294=DIRECTION('ref_axis',(6.12323399573677E-17,0.,1.));
#5295=DIRECTION('center_axis',(0.,1.,0.));
#5296=DIRECTION('ref_axis',(6.12323399573677E-17,0.,1.));
#6465=CARTESIAN_POINT('',(0.,0.,0.));
#6466=CARTESIAN_POINT('Origin',(-3.53553390593273,-3.,117.867942062963));
#6467=CARTESIAN_POINT('',(-3.53553390593273,-3.,117.867942062963));
#6468=CARTESIAN_POINT('',(-23.9002092041053,-3.,138.232617361136));
#6469=CARTESIAN_POINT('',(-1.76776695296637,-3.,116.100175109997));
#6470=CARTESIAN_POINT('',(-3.53553390593273,-2.9,117.867942062963));
#6471=CARTESIAN_POINT('',(-3.53553390593273,-3.,117.867942062963));
#6472=CARTESIAN_POINT('',(-23.9002092041053,-2.9,138.232617361136));
#6473=CARTESIAN_POINT('',(-1.76776695296637,-2.9,116.100175109997));
#6474=CARTESIAN_POINT('',(-23.9002092041053,-3.,138.232617361136));
#6475=CARTESIAN_POINT('Origin',(-33.8,-3.,114.33240815703));
#6476=CARTESIAN_POINT('',(-33.8,-3.,114.33240815703));
#6477=CARTESIAN_POINT('',(-5.,-3.,114.33240815703));
#6478=CARTESIAN_POINT('',(-16.9,-3.,114.33240815703));
#6479=CARTESIAN_POINT('',(-33.8,-2.9,114.33240815703));
#6480=CARTESIAN_POINT('',(-33.8,-3.,114.33240815703));
#6481=CARTESIAN_POINT('',(-5.,-2.9,114.33240815703));
#6482=CARTESIAN_POINT('',(-16.9,-2.9,114.33240815703));
#6483=CARTESIAN_POINT('',(-5.,-3.,114.33240815703));
#6484=CARTESIAN_POINT('Origin',(0.,-3.,114.33240815703));
#6485=CARTESIAN_POINT('Origin',(0.,-3.,114.33240815703));
#6486=CARTESIAN_POINT('Origin',(0.,-3.,114.33240815703));
#6487=CARTESIAN_POINT('',(-28.5450224208979,-3.,119.536825430901));
#6488=CARTESIAN_POINT('Origin',(-28.5450224208979,-3.,120.636825430901));
#6489=CARTESIAN_POINT('',(-23.9595659283167,-3.,129.980637397738));
#6490=CARTESIAN_POINT('Origin',(-23.9595659283167,-3.,131.080637397738));
#6491=CARTESIAN_POINT('Origin',(-28.5450224208979,-3.,120.636825430901));
#6492=CARTESIAN_POINT('',(-28.5450224208979,-3.5,119.536825430901));
#6493=CARTESIAN_POINT('Origin',(-28.5450224208979,-3.5,120.636825430901));
#6494=CARTESIAN_POINT('',(-28.5450224208979,-3.,119.536825430901));
#6495=CARTESIAN_POINT('Origin',(-28.5450224208979,-3.5,120.636825430901));
#6496=CARTESIAN_POINT('Origin',(-23.9595659283167,-3.,131.080637397738));
#6497=CARTESIAN_POINT('',(-23.9595659283167,-3.5,129.980637397738));
#6498=CARTESIAN_POINT('Origin',(-23.9595659283167,-3.5,131.080637397738));
#6499=CARTESIAN_POINT('',(-23.9595659283167,-3.,129.980637397738));
#6500=CARTESIAN_POINT('Origin',(-23.9595659283167,-3.5,131.080637397738));
#6501=CARTESIAN_POINT('Origin',(0.,-3.,114.33240815703));
#6502=CARTESIAN_POINT('Origin',(0.,-2.9,114.33240815703));
#6503=CARTESIAN_POINT('Origin',(0.,-3.,114.33240815703));
#6504=CARTESIAN_POINT('Origin',(0.,-2.9,114.33240815703));
#6505=CARTESIAN_POINT('Origin',(0.,-2.9,114.33240815703));
#6732=UNCERTAINTY_MEASURE_WITH_UNIT(LENGTH_MEASURE(0.01),#6754,
'DISTANCE_ACCURACY_VALUE',
'Maximum model space distance between geometric entities at asserted c
onnectivities');
#6738=UNCERTAINTY_MEASURE_WITH_UNIT(LENGTH_MEASURE(0.01),#6754,
'DISTANCE_ACCURACY_VALUE',
'Maximum model space distance between geometric entities at asserted c
onnectivities');
#6747=(
GEOMETRIC_REPRESENTATION_CONTEXT(3)
GLOBAL_UNCERTAINTY_ASSIGNED_CONTEXT((#6732))
GLOBAL_UNIT_ASSIGNED_CONTEXT((#6754,#6756,#6757))
REPRESENTATION_CONTEXT('','3D')
);
#6753=(
GEOMETRIC_REPRESENTATION_CONTEXT(3)
GLOBAL_UNCERTAINTY_ASSIGNED_CONTEXT((#6738))
GLOBAL_UNIT_ASSIGNED_CONTEXT((#6754,#6756,#6757))
REPRESENTATION_CONTEXT('','3D')
);
#6754=(
LENGTH_UNIT()
NAMED_UNIT(*)
SI_UNIT(.MILLI.,.METRE.)
);
#6756=(
NAMED_UNIT(*)
PLANE_ANGLE_UNIT()
SI_UNIT($,.RADIAN.)
);
#6757=(
NAMED_UNIT(*)
SI_UNIT($,.STERADIAN.)
SOLID_ANGLE_UNIT()
);
#6766=SHAPE_DEFINITION_REPRESENTATION(#6780,#6807);
#6780=PRODUCT_DEFINITION_SHAPE('',$,#6822);
#6807=SHAPE_REPRESENTATION('',(#4238),#6747);
#6813=PRODUCT_DEFINITION_CONTEXT('part definition',#6857,'design');
#6822=PRODUCT_DEFINITION('Blade_03','Blade_03',#6836,#6813);
#6836=PRODUCT_DEFINITION_FORMATION('',$,#6867);
#6857=APPLICATION_CONTEXT(
'Core Data for Automotive Mechanical Design Process');
#6858=PRODUCT_CONTEXT('part definition',#6857,'mechanical');
#6867=PRODUCT('Blade_03','Blade_03',$,(#6858));
#6908=COLOUR_RGB('Sky Blue',0.24,0.69,0.87);
#6909=FILL_AREA_STYLE_COLOUR('',#6908);
#6910=FILL_AREA_STYLE('',(#6909));
#6911=SURFACE_STYLE_FILL_AREA(#6910);
#6912=SURFACE_SIDE_STYLE('',(#6911));
#6913=SURFACE_STYLE_USAGE(.BOTH.,#6912);
#6914=PRESENTATION_STYLE_ASSIGNMENT((#6913));
ENDSEC;
END-ISO-10303-21;
